ISO-10303-21;
HEADER;
/* Generated by software containing ST-Developer
 * from STEP Tools, Inc. (www.steptools.com) 
 */

FILE_DESCRIPTION(
/* description */ ('Hand-operated arbor press'),
/* implementation_level */ '2;1');

FILE_NAME(
/* name */ 'Flat Washer - M6.step',
/* time_stamp */ '2026-10-28T03:25:25-07:00',
/* author */ (''),
/* organization */ (''),
/* preprocessor_version */ 'ST-DEVELOPER v20.2',
/* originating_system */ 'Autodesk Translation Framework v15.17.0.0',
/* authorisation */ '');

FILE_SCHEMA (('AUTOMOTIVE_DESIGN { 1 0 10303 214 3 1 1 }'));
ENDSEC;

DATA;
#10=MECHANICAL_DESIGN_GEOMETRIC_PRESENTATION_REPRESENTATION('',(#631),#32751);
#540=SHAPE_REPRESENTATION_RELATIONSHIP('SRR','None',#32972,#582);
#582=ADVANCED_BREP_SHAPE_REPRESENTATION('',(#678),#32746);
#631=STYLED_ITEM('',(#33249),#678);
#678=MANIFOLD_SOLID_BREP('Body1',#12530);
#843=FACE_BOUND('',#2779,.T.);
#844=FACE_BOUND('',#2781,.T.);
#1267=PLANE('',#14023);
#1268=PLANE('',#14024);
#1932=FACE_OUTER_BOUND('',#2776,.T.);
#1933=FACE_OUTER_BOUND('',#2777,.T.);
#1934=FACE_OUTER_BOUND('',#2778,.T.);
#1935=FACE_OUTER_BOUND('',#2780,.T.);
#2776=EDGE_LOOP('',(#11490,#11491,#11492,#11493));
#2777=EDGE_LOOP('',(#11494,#11495,#11496,#11497));
#2778=EDGE_LOOP('',(#11498));
#2779=EDGE_LOOP('',(#11499));
#2780=EDGE_LOOP('',(#11500));
#2781=EDGE_LOOP('',(#11501));
#3943=LINE('',#32420,#5114);
#3944=LINE('',#32426,#5115);
#5114=VECTOR('',#17314,0.32);
#5115=VECTOR('',#17321,0.6);
#5532=CIRCLE('',#14018,0.32);
#5533=CIRCLE('',#14019,0.32);
#5534=CIRCLE('',#14021,0.6);
#5535=CIRCLE('',#14022,0.6);
#6617=VERTEX_POINT('',#32417);
#6618=VERTEX_POINT('',#32419);
#6619=VERTEX_POINT('',#32423);
#6620=VERTEX_POINT('',#32425);
#8248=EDGE_CURVE('',#6617,#6617,#5532,.T.);
#8249=EDGE_CURVE('',#6617,#6618,#3943,.T.);
#8250=EDGE_CURVE('',#6618,#6618,#5533,.T.);
#8251=EDGE_CURVE('',#6619,#6619,#5534,.T.);
#8252=EDGE_CURVE('',#6619,#6620,#3944,.T.);
#8253=EDGE_CURVE('',#6620,#6620,#5535,.T.);
#11490=ORIENTED_EDGE('',*,*,#8248,.F.);
#11491=ORIENTED_EDGE('',*,*,#8249,.T.);
#11492=ORIENTED_EDGE('',*,*,#8250,.T.);
#11493=ORIENTED_EDGE('',*,*,#8249,.F.);
#11494=ORIENTED_EDGE('',*,*,#8251,.F.);
#11495=ORIENTED_EDGE('',*,*,#8252,.T.);
#11496=ORIENTED_EDGE('',*,*,#8253,.T.);
#11497=ORIENTED_EDGE('',*,*,#8252,.F.);
#11498=ORIENTED_EDGE('',*,*,#8251,.T.);
#11499=ORIENTED_EDGE('',*,*,#8248,.T.);
#11500=ORIENTED_EDGE('',*,*,#8253,.F.);
#11501=ORIENTED_EDGE('',*,*,#8250,.F.);
#11794=CYLINDRICAL_SURFACE('',#14017,0.32);
#11795=CYLINDRICAL_SURFACE('',#14020,0.6);
#12441=ADVANCED_FACE('',(#1932),#11794,.F.);
#12442=ADVANCED_FACE('',(#1933),#11795,.T.);
#12443=ADVANCED_FACE('',(#1934,#843),#1267,.T.);
#12444=ADVANCED_FACE('',(#1935,#844),#1268,.F.);
#12530=CLOSED_SHELL('',(#12441,#12442,#12443,#12444));
#14016=AXIS2_PLACEMENT_3D('',#32415,#17308,#17309);
#14017=AXIS2_PLACEMENT_3D('',#32416,#17310,#17311);
#14018=AXIS2_PLACEMENT_3D('',#32418,#17312,#17313);
#14019=AXIS2_PLACEMENT_3D('',#32421,#17315,#17316);
#14020=AXIS2_PLACEMENT_3D('',#32422,#17317,#17318);
#14021=AXIS2_PLACEMENT_3D('',#32424,#17319,#17320);
#14022=AXIS2_PLACEMENT_3D('',#32427,#17322,#17323);
#14023=AXIS2_PLACEMENT_3D('',#32428,#17324,#17325);
#14024=AXIS2_PLACEMENT_3D('',#32429,#17326,#17327);
#17308=DIRECTION('axis',(0.,0.,1.));
#17309=DIRECTION('refdir',(1.,0.,0.));
#17310=DIRECTION('center_axis',(0.,1.,0.));
#17311=DIRECTION('ref_axis',(1.,0.,0.));
#17312=DIRECTION('center_axis',(0.,-1.,0.));
#17313=DIRECTION('ref_axis',(1.,0.,0.));
#17314=DIRECTION('',(0.,-1.,0.));
#17315=DIRECTION('center_axis',(0.,-1.,0.));
#17316=DIRECTION('ref_axis',(1.,0.,0.));
#17317=DIRECTION('center_axis',(0.,1.,0.));
#17318=DIRECTION('ref_axis',(1.,0.,0.));
#17319=DIRECTION('center_axis',(0.,1.,0.));
#17320=DIRECTION('ref_axis',(1.,0.,0.));
#17321=DIRECTION('',(0.,-1.,0.));
#17322=DIRECTION('center_axis',(0.,1.,0.));
#17323=DIRECTION('ref_axis',(1.,0.,0.));
#17324=DIRECTION('center_axis',(0.,1.,0.));
#17325=DIRECTION('ref_axis',(1.,0.,0.));
#17326=DIRECTION('center_axis',(0.,1.,0.));
#17327=DIRECTION('ref_axis',(1.,0.,0.));
#32415=CARTESIAN_POINT('',(0.,0.,0.));
#32416=CARTESIAN_POINT('Origin',(0.,0.,0.));
#32417=CARTESIAN_POINT('',(-0.32,0.16,3.91886975727153E-17));
#32418=CARTESIAN_POINT('Origin',(0.,0.16,0.));
#32419=CARTESIAN_POINT('',(-0.32,0.,3.91886975727153E-17));
#32420=CARTESIAN_POINT('',(-0.32,0.,3.91886975727153E-17));
#32421=CARTESIAN_POINT('Origin',(0.,0.,0.));
#32422=CARTESIAN_POINT('Origin',(0.,0.,0.));
#32423=CARTESIAN_POINT('',(-0.6,0.16,7.34788079488412E-17));
#32424=CARTESIAN_POINT('Origin',(0.,0.16,0.));
#32425=CARTESIAN_POINT('',(-0.6,0.,7.34788079488412E-17));
#32426=CARTESIAN_POINT('',(-0.6,0.,7.34788079488412E-17));
#32427=CARTESIAN_POINT('Origin',(0.,0.,0.));
#32428=CARTESIAN_POINT('Origin',(0.,0.16,0.));
#32429=CARTESIAN_POINT('Origin',(0.,0.,0.));
#32697=UNCERTAINTY_MEASURE_WITH_UNIT(LENGTH_MEASURE(0.001),#32752,
'DISTANCE_ACCURACY_VALUE',
'Maximum model space distance between geometric entities at asserted c
onnectivities');
#32702=UNCERTAINTY_MEASURE_WITH_UNIT(LENGTH_MEASURE(0.001),#32752,
'DISTANCE_ACCURACY_VALUE',
'Maximum model space distance between geometric entities at asserted c
onnectivities');
#32746=(
GEOMETRIC_REPRESENTATION_CONTEXT(3)
GLOBAL_UNCERTAINTY_ASSIGNED_CONTEXT((#32697))
GLOBAL_UNIT_ASSIGNED_CONTEXT((#32752,#32754,#32755))
REPRESENTATION_CONTEXT('','3D')
);
#32751=(
GEOMETRIC_REPRESENTATION_CONTEXT(3)
GLOBAL_UNCERTAINTY_ASSIGNED_CONTEXT((#32702))
GLOBAL_UNIT_ASSIGNED_CONTEXT((#32752,#32754,#32755))
REPRESENTATION_CONTEXT('','3D')
);
#32752=(
LENGTH_UNIT()
NAMED_UNIT(*)
SI_UNIT(.CENTI.,.METRE.)
);
#32754=(
NAMED_UNIT(*)
PLANE_ANGLE_UNIT()
SI_UNIT($,.RADIAN.)
);
#32755=(
NAMED_UNIT(*)
SI_UNIT($,.STERADIAN.)
SOLID_ANGLE_UNIT()
);
#32799=SHAPE_DEFINITION_REPRESENTATION(#32856,#32972);
#32856=PRODUCT_DEFINITION_SHAPE('',$,#33021);
#32972=SHAPE_REPRESENTATION('',(#14016),#32746);
#32977=PRODUCT_DEFINITION_CONTEXT('part definition',#33123,'design');
#33021=PRODUCT_DEFINITION('Flat Washer - M6','Flat Washer - M6',#33069,
#32977);
#33069=PRODUCT_DEFINITION_FORMATION('',$,#33168);
#33123=APPLICATION_CONTEXT(
'Core Data for Automotive Mechanical Design Process');
#33124=PRODUCT_CONTEXT('part definition',#33123,'mechanical');
#33168=PRODUCT('Flat Washer - M6','Flat Washer - M6','Flat Washer - M6',
(#33124));
#33243=COLOUR_RGB('Black',0.12,0.14,0.17);
#33244=FILL_AREA_STYLE_COLOUR('',#33243);
#33245=FILL_AREA_STYLE('',(#33244));
#33246=SURFACE_STYLE_FILL_AREA(#33245);
#33247=SURFACE_SIDE_STYLE('',(#33246));
#33248=SURFACE_STYLE_USAGE(.BOTH.,#33247);
#33249=PRESENTATION_STYLE_ASSIGNMENT((#33248));
ENDSEC;
END-ISO-10303-21;
